ISO-10303-21;
HEADER;
FILE_DESCRIPTION (('STEP AP214'),
    '1' );
FILE_NAME ('hex structural bolt gradec short_iso_ISO 7412 - M16 x 45 --- 26-WN.step',
    '2026-10-21T17:50:41',
    ( '' ),
    ( '' ),
    'SwSTEP 2.0',
    'SolidWorks 2026',
    '' );
FILE_SCHEMA (( 'AUTOMOTIVE_DESIGN' ));
ENDSEC;

DATA;
#95=CARTESIAN_POINT ( 'NONE',  ( 9.199999999999999289, -7.794228634059966687, -13.49999999999999822 ) ) ;
#105=ORIENTED_EDGE ( 'NONE', *, *, #3853, .F. ) ;
#114=EDGE_CURVE ( 'NONE', #27996, #34376, #12253, .T. ) ;
#116=CARTESIAN_POINT ( 'NONE',  ( 9.199999999999999289, 7.794228634059941818, 13.49999999999999645 ) ) ;
#129=CARTESIAN_POINT ( 'NONE',  ( 9.199999999999999289, -7.794228634059966687, -13.49999999999999822 ) ) ;
#155=DIRECTION ( 'NONE',  ( 1.000000000000000000, 0.000000000000000000, 0.000000000000000000 ) ) ;
#202=B_SPLINE_CURVE_WITH_KNOTS ( 'NONE', 3,
 ( #7828, #4974, #32217, #8004, #26873, #2488, #32384, #18882 ),
 .UNSPECIFIED., .F., .F.,
 ( 4, 2, 2, 4 ),
 ( 0.007886720825438783139, 0.009850969036563994238, 0.01181521724768920534, 0.01574371366993962407 ),
 .UNSPECIFIED. ) ;
#212=DIRECTION ( 'NONE',  ( 0.000000000000000000, 0.000000000000000000, 1.000000000000000000 ) ) ;
#237=AXIS2_PLACEMENT_3D ( 'NONE', #28026, #9683, #31396 ) ;
#274=DIRECTION ( 'NONE',  ( 0.000000000000000000, 0.000000000000000000, 1.000000000000000000 ) ) ;
#305=LINE ( 'NONE', #11698, #310 ) ;
#310=VECTOR ( 'NONE', #22368, 999.9999999999998863 ) ;
#385=EDGE_LOOP ( 'NONE', ( #22303, #2960 ) ) ;
#438=ORIENTED_EDGE ( 'NONE', *, *, #25737, .T. ) ;
#458=EDGE_CURVE ( 'NONE', #20784, #34333, #22819, .T. ) ;
#475=ORIENTED_EDGE ( 'NONE', *, *, #20470, .F. ) ;
#480=EDGE_CURVE ( 'NONE', #32964, #14283, #33981, .T. ) ;
#505=ORIENTED_EDGE ( 'NONE', *, *, #3408, .T. ) ;
#620=CIRCLE ( 'NONE', #9710, 13.49999999999999822 ) ;
#647=ORIENTED_EDGE ( 'NONE', *, *, #9770, .F. ) ;
#670=EDGE_CURVE ( 'NONE', #3150, #31908, #29334, .T. ) ;
#676=CARTESIAN_POINT ( 'NONE',  ( 55.00000000000000711, 9.122700168548420677E-16, -6.898500000000000298 ) ) ;
#704=ORIENTED_EDGE ( 'NONE', *, *, #7401, .F. ) ;
#755=CARTESIAN_POINT ( 'NONE',  ( -1.025333382651330166E-15, 0.6596962799366378194, 13.49999999999999645 ) ) ;
#756=UNCERTAINTY_MEASURE_WITH_UNIT (LENGTH_MEASURE( 1.000000000000000082E-05 ), #23264, 'distance_accuracy_value', 'NONE');
#861=ORIENTED_EDGE ( 'NONE', *, *, #7933, .F. ) ;
#934=CARTESIAN_POINT ( 'NONE',  ( 1.205771365940041528, 7.794228634059941818, 13.49999999999999645 ) ) ;
#936=CARTESIAN_POINT ( 'NONE',  ( 53.89849999999999852, 9.797174393178825657E-16, -8.000000000000000000 ) ) ;
#982=DIRECTION ( 'NONE',  ( -1.000000000000000000, -0.000000000000000000, 0.000000000000000000 ) ) ;
#1018=CARTESIAN_POINT ( 'NONE',  ( 0.000000000000000000, 0.000000000000000000, -13.49999999999999822 ) ) ;
#1056=CARTESIAN_POINT ( 'NONE',  ( 0.000000000000000000, 0.000000000000000000, 0.000000000000000000 ) ) ;
#1102=CARTESIAN_POINT ( 'NONE',  ( 9.199999999999999289, 7.794228634059941818, 13.49999999999999645 ) ) ;
#1282=AXIS2_PLACEMENT_3D ( 'NONE', #25350, #982, #13983 ) ;
#1288=CARTESIAN_POINT ( 'NONE',  ( 0.8377008405913606293, -14.95094041744786928, 1.104211576045298404 ) ) ;
#1347=CARTESIAN_POINT ( 'NONE',  ( 0.000000000000000000, 0.000000000000000000, 0.000000000000000000 ) ) ;
#1370=EDGE_CURVE ( 'NONE', #20728, #13531, #12820, .T. ) ;
#1421=VECTOR ( 'NONE', #19434, 1000.000000000000000 ) ;
#1465=ORIENTED_EDGE ( 'NONE', *, *, #5762, .F. ) ;
#1480=CARTESIAN_POINT ( 'NONE',  ( 10.00000000000000000, 1.653273178848927064E-15, -13.50000000000000178 ) ) ;
#1532=CARTESIAN_POINT ( 'NONE',  ( 0.000000000000000000, 0.000000000000000000, 0.000000000000000000 ) ) ;
#1715=DIRECTION ( 'NONE',  ( 1.000000000000000000, 0.000000000000000000, -0.000000000000000000 ) ) ;
#1758=MECHANICAL_DESIGN_GEOMETRIC_PRESENTATION_REPRESENTATION('',(#9156),#23929);
#1901=CARTESIAN_POINT ( 'NONE',  ( 10.00000000000000000, 0.000000000000000000, 13.50000000000000178 ) ) ;
#1908=FACE_OUTER_BOUND ( 'NONE', #32205, .T. ) ;
#1946=VECTOR ( 'NONE', #3218, 999.9999999999998863 ) ;
#2177=DIRECTION ( 'NONE',  ( -1.000000000000000000, -0.000000000000000000, -0.000000000000000000 ) ) ;
#2182=PLANE ( 'NONE',  #19747 ) ;
#2198=ADVANCED_FACE ( 'NONE', ( #6004 ), #13911, .T. ) ;
#2200=DIRECTION ( 'NONE',  ( 0.000000000000000000, 0.000000000000000000, 1.000000000000000000 ) ) ;
#2220=FACE_OUTER_BOUND ( 'NONE', #13490, .T. ) ;
#2337=CARTESIAN_POINT ( 'NONE',  ( 9.199999999999999289, 0.000000000000000000, 0.000000000000000000 ) ) ;
#2378=VECTOR ( 'NONE', #15660, 1000.000000000000000 ) ;
#2403=CARTESIAN_POINT ( 'NONE',  ( 9.199999999999999289, 11.69134295108991672, 6.750000000000011546 ) ) ;
#2440=CARTESIAN_POINT ( 'NONE',  ( 53.89849999999999852, 0.000000000000000000, 0.000000000000000000 ) ) ;
#2484=CARTESIAN_POINT ( 'NONE',  ( 10.00000000000000000, 7.794228634059932048, -13.49999999999999822 ) ) ;
#2488=CARTESIAN_POINT ( 'NONE',  ( 0.5355294694855877724, -14.31130214556279867, -2.212097561415799607 ) ) ;
#2500=PRODUCT_DEFINITION_CONTEXT ( 'detailed design', #4164, 'design' ) ;
#2519=LINE ( 'NONE', #18218, #24681 ) ;
#2553=LINE ( 'NONE', #21254, #26975 ) ;
#2653=AXIS2_PLACEMENT_3D ( 'NONE', #2484, #24015, #34897 ) ;
#2686=ORIENTED_EDGE ( 'NONE', *, *, #670, .T. ) ;
#2721=ORIENTED_EDGE ( 'NONE', *, *, #6742, .T. ) ;
#2755=CARTESIAN_POINT ( 'NONE',  ( 9.199999999999999289, 0.000000000000000000, 0.000000000000000000 ) ) ;
#2815=CARTESIAN_POINT ( 'NONE',  ( 0.000000000000000000, 0.000000000000000000, 0.000000000000000000 ) ) ;
#2839=ORIENTED_EDGE ( 'NONE', *, *, #27763, .T. ) ;
#2857=LINE ( 'NONE', #22093, #1421 ) ;
#2891=CIRCLE ( 'NONE', #13155, 13.50000000000000178 ) ;
#2960=ORIENTED_EDGE ( 'NONE', *, *, #5762, .T. ) ;
#2972=DIRECTION ( 'NONE',  ( 0.000000000000000000, 0.000000000000000000, -1.000000000000000000 ) ) ;
#3020=CARTESIAN_POINT ( 'NONE',  ( 9.199999999999999289, -7.794228634059937377, 13.50000000000000000 ) ) ;
#3096=CONICAL_SURFACE ( 'NONE', #23006, 13.50000000000000000, 1.047197551196600296 ) ;
#3150=VERTEX_POINT ( 'NONE', #20353 ) ;
#3156=DIRECTION ( 'NONE',  ( -1.000000000000000000, -0.000000000000000000, -0.000000000000000000 ) ) ;
#3218=DIRECTION ( 'NONE',  ( 0.000000000000000000, -0.5000000000000008882, 0.8660254037844382635 ) ) ;
#3230=PLANE ( 'NONE',  #15173 ) ;
#3239=CARTESIAN_POINT ( 'NONE',  ( 0.02815752724700520265, 1.322857909621847350, 13.50000000000000000 ) ) ;
#3286=EDGE_LOOP ( 'NONE', ( #31431, #5977, #13422 ) ) ;
#3336=CARTESIAN_POINT ( 'NONE',  ( 9.199999999999999289, 15.58845726811990495, 0.000000000000000000 ) ) ;
#3337=ORIENTED_EDGE ( 'NONE', *, *, #21203, .F. ) ;
#3408=EDGE_CURVE ( 'NONE', #17794, #20784, #18679, .T. ) ;
#3411=CARTESIAN_POINT ( 'NONE',  ( 0.5390048853414316499, 5.257018938344287129, 13.49999999999999822 ) ) ;
#3572=DIRECTION ( 'NONE',  ( -1.000000000000000000, -0.000000000000000000, -0.000000000000000000 ) ) ;
#3711=FACE_OUTER_BOUND ( 'NONE', #5844, .T. ) ;
#3741=CARTESIAN_POINT ( 'NONE',  ( 0.000000000000000000, 0.000000000000000000, 13.50000000000000178 ) ) ;
#3755=DIRECTION ( 'NONE',  ( 0.000000000000000000, 0.000000000000000000, -1.000000000000000000 ) ) ;
#3799=CARTESIAN_POINT ( 'NONE',  ( 0.5355294694855760040, 14.31130214556277735, 2.212097561415798719 ) ) ;
#3809=DIRECTION ( 'NONE',  ( 1.000000000000000000, 0.000000000000000000, 0.000000000000000000 ) ) ;
#3853=EDGE_CURVE ( 'NONE', #12566, #3150, #14744, .T. ) ;
#3854=FACE_OUTER_BOUND ( 'NONE', #17500, .T. ) ;
#3924=CARTESIAN_POINT ( 'NONE',  ( 0.000000000000000000, 11.69134295108991495, 6.750000000000012434 ) ) ;
#4139=FACE_OUTER_BOUND ( 'NONE', #385, .T. ) ;
#4143=CARTESIAN_POINT ( 'NONE',  ( 0.1387913946425727574, 13.01149508916974895, 4.463429423125059969 ) ) ;
#4164=APPLICATION_CONTEXT ( 'automotive_design' ) ;
#4165=ADVANCED_FACE ( 'NONE', ( #34621 ), #13029, .T. ) ;
#4208=CONICAL_SURFACE ( 'NONE', #15591, 13.50000000000000000, 1.047197551196600296 ) ;
#4283=CARTESIAN_POINT ( 'NONE',  ( 0.000000000000000000, -11.69134295108990607, 6.750000000000024869 ) ) ;
#4305=CARTESIAN_POINT ( 'NONE',  ( -9.419006373467819770E-16, -1.318430554023032553, 13.49999999999999822 ) ) ;
#4368=PLANE ( 'NONE',  #34739 ) ;
#4411=B_SPLINE_CURVE_WITH_KNOTS ( 'NONE', 3,
 ( #18324, #26485, #12973, #29157, #4753, #18505 ),
 .UNSPECIFIED., .F., .F.,
 ( 4, 2, 4 ),
 ( 0.04390953152370602464, 0.04785567665046381453, 0.05180182177722160441 ),
 .UNSPECIFIED. ) ;
#4525=CARTESIAN_POINT ( 'NONE',  ( 0.1387913946425762823, -10.37119081301008272, 9.036570576874970229 ) ) ;
#4533=( NAMED_UNIT ( * ) PLANE_ANGLE_UNIT ( ) SI_UNIT ( $, .RADIAN. ) );
#4563=CARTESIAN_POINT ( 'NONE',  ( 10.00000000000000000, 9.797174393178825657E-16, -8.000000000000000000 ) ) ;
#4565=ORIENTED_EDGE ( 'NONE', *, *, #7900, .T. ) ;
#4595=CARTESIAN_POINT ( 'NONE',  ( 9.199999999999999289, 0.000000000000000000, 0.000000000000000000 ) ) ;
#4618=CARTESIAN_POINT ( 'NONE',  ( 1.205771365940050410, 15.58845726811990495, 1.140844902514640588E-16 ) ) ;
#4687=ORIENTED_EDGE ( 'NONE', *, *, #12173, .F. ) ;
#4706=VECTOR ( 'NONE', #32700, 1000.000000000000000 ) ;
#4753=CARTESIAN_POINT ( 'NONE',  ( 0.8394537150704712847, -6.525267068029305229, -13.49999999999999822 ) ) ;
#4811=AXIS2_PLACEMENT_3D ( 'NONE', #7297, #21378, #2972 ) ;
#4837=CARTESIAN_POINT ( 'NONE',  ( 9.199999999999999289, 13.50000000000000178, 0.000000000000000000 ) ) ;
#4957=ORIENTED_EDGE ( 'NONE', *, *, #7933, .T. ) ;
#4974=CARTESIAN_POINT ( 'NONE',  ( 3.754050022231059892E-15, -12.02207793746707765, -6.177150199754210647 ) ) ;
#4985=CARTESIAN_POINT ( 'NONE',  ( 55.00000000000000711, 0.000000000000000000, 6.898500000000000298 ) ) ;
#4990=( NAMED_UNIT ( * ) SI_UNIT ( $, .STERADIAN. ) SOLID_ANGLE_UNIT ( ) );
#5053=LINE ( 'NONE', #16470, #25052 ) ;
#5111=LINE ( 'NONE', #21843, #9888 ) ;
#5116=LINE ( 'NONE', #22035, #19055 ) ;
#5125=DIRECTION ( 'NONE',  ( 0.000000000000000000, 0.000000000000000000, 1.000000000000000000 ) ) ;
#5296=AXIS2_PLACEMENT_3D ( 'NONE', #33363, #28555, #22870 ) ;
#5312=DIRECTION ( 'NONE',  ( 0.000000000000000000, 0.000000000000000000, 1.000000000000000000 ) ) ;
#5314=EDGE_LOOP ( 'NONE', ( #23751, #438, #34233, #23436, #14022, #30155 ) ) ;
#5317=ADVANCED_FACE ( 'NONE', ( #22237 ), #25426, .T. ) ;
#5335=FACE_OUTER_BOUND ( 'NONE', #7595, .T. ) ;
#5343=ORIENTED_EDGE ( 'NONE', *, *, #7900, .F. ) ;
#5344=CIRCLE ( 'NONE', #7633, 13.50000000000000178 ) ;
#5364=DIRECTION ( 'NONE',  ( 0.000000000000000000, 0.000000000000000000, -1.000000000000000000 ) ) ;
#5439=CARTESIAN_POINT ( 'NONE',  ( 0.000000000000000000, -11.69134295108991672, -6.750000000000007105 ) ) ;
#5546=ORIENTED_EDGE ( 'NONE', *, *, #16139, .F. ) ;
#5558=ORIENTED_EDGE ( 'NONE', *, *, #6742, .F. ) ;
#5574=DIRECTION ( 'NONE',  ( -1.000000000000000000, -0.000000000000000000, -0.000000000000000000 ) ) ;
#5613=PLANE ( 'NONE',  #10544 ) ;
#5657=LINE ( 'NONE', #13521, #21435 ) ;
#5710=CARTESIAN_POINT ( 'NONE',  ( 53.89849999999999852, 0.000000000000000000, 8.000000000000000000 ) ) ;
#5762=EDGE_CURVE ( 'NONE', #19390, #14536, #5344, .T. ) ;
#5784=LINE ( 'NONE', #116, #10257 ) ;
#5799=CARTESIAN_POINT ( 'NONE',  ( 0.5390048853417120922, 5.257018938344060643, -13.49999999999999645 ) ) ;
#5844=EDGE_LOOP ( 'NONE', ( #13677, #15893, #34133, #9914 ) ) ;
#5849=VERTEX_POINT ( 'NONE', #11784 ) ;
#5876=LINE ( 'NONE', #16777, #1946 ) ;
#5896=CARTESIAN_POINT ( 'NONE',  ( 9.199999999999999289, 0.000000000000000000, 0.000000000000000000 ) ) ;
#5915=EDGE_CURVE ( 'NONE', #31908, #9042, #5876, .T. ) ;
#5977=ORIENTED_EDGE ( 'NONE', *, *, #13076, .T. ) ;
#5985=APPLICATION_CONTEXT ( 'automotive_design' ) ;
#6004=FACE_OUTER_BOUND ( 'NONE', #3286, .T. ) ;
#6021=DIRECTION ( 'NONE',  ( 0.000000000000000000, 0.000000000000000000, 1.000000000000000000 ) ) ;
#6027=CARTESIAN_POINT ( 'NONE',  ( 0.000000000000000000, 0.000000000000000000, 0.000000000000000000 ) ) ;
#6065=CARTESIAN_POINT ( 'NONE',  ( -7.433561145103738198E-15, 11.02739026146940304, 7.899999792244740249 ) ) ;
#6073=CARTESIAN_POINT ( 'NONE',  ( 9.199999999999999289, 7.794228634059932048, -13.49999999999999822 ) ) ;
#6138=PLANE ( 'NONE',  #28383 ) ;
#6208=EDGE_CURVE ( 'NONE', #34376, #8985, #13523, .T. ) ;
#6270=ORIENTED_EDGE ( 'NONE', *, *, #29153, .T. ) ;
#6312=DIRECTION ( 'NONE',  ( -0.000000000000000000, 0.8660254037844383745, 0.5000000000000005551 ) ) ;
#6377=DIRECTION ( 'NONE',  ( -1.000000000000000000, -0.000000000000000000, -0.000000000000000000 ) ) ;
#6461=CARTESIAN_POINT ( 'NONE',  ( 9.199999999999999289, 7.794228634059932048, -13.49999999999999822 ) ) ;
#6467=CARTESIAN_POINT ( 'NONE',  ( 0.8386200322165776599, 14.95253250404440237, 1.101454001170010244 ) ) ;
#6623=ORIENTED_EDGE ( 'NONE', *, *, #13076, .F. ) ;
#6639=CARTESIAN_POINT ( 'NONE',  ( 9.199999999999999289, 0.000000000000000000, -13.50000000000000000 ) ) ;
#6693=AXIS2_PLACEMENT_3D ( 'NONE', #8337, #29531, #5125 ) ;
#6742=EDGE_CURVE ( 'NONE', #34333, #17794, #305, .T. ) ;
#7054=ORIENTED_EDGE ( 'NONE', *, *, #11010, .F. ) ;
#7103=FACE_OUTER_BOUND ( 'NONE', #32827, .T. ) ;
#7120=DIRECTION ( 'NONE',  ( 1.000000000000000000, 0.000000000000000000, 0.000000000000000000 ) ) ;
#7128=B_SPLINE_CURVE_WITH_KNOTS ( 'NONE', 3,
 ( #20700, #23200, #33875, #28704, #4305, #34044 ),
 .UNSPECIFIED., .F., .F.,
 ( 4, 2, 4 ),
 ( 0.01435361776844886611, 0.01829828670248722505, 0.02224295563652558400 ),
 .UNSPECIFIED. ) ;
#7195=DIRECTION ( 'NONE',  ( 0.000000000000000000, 0.000000000000000000, -1.000000000000000000 ) ) ;
#7217=AXIS2_PLACEMENT_3D ( 'NONE', #12613, #15822, #23637 ) ;
#7297=CARTESIAN_POINT ( 'NONE',  ( 9.199999999999999289, 13.50000000000000178, 0.000000000000000000 ) ) ;
#7300=CARTESIAN_POINT ( 'NONE',  ( 0.1149164202474758090, 13.01099471650157824, -4.464296094009046811 ) ) ;
#7401=EDGE_CURVE ( 'NONE', #17794, #35009, #30688, .T. ) ;
#7421=AXIS2_PLACEMENT_3D ( 'NONE', #10407, #5574, #27127 ) ;
#7442=CIRCLE ( 'NONE', #18860, 13.49999999999999822 ) ;
#7459=AXIS2_PLACEMENT_3D ( 'NONE', #24460, #15967, #13458 ) ;
#7489=PRODUCT_CONTEXT ( 'NONE', #5985, 'mechanical' ) ;
#7574=CARTESIAN_POINT ( 'NONE',  ( 1.205771365940040196, 7.794228634059932048, -13.49999999999999822 ) ) ;
#7587=ORIENTED_EDGE ( 'NONE', *, *, #19452, .F. ) ;
#7595=EDGE_LOOP ( 'NONE', ( #25884, #25189, #19260 ) ) ;
#7620=B_SPLINE_CURVE_WITH_KNOTS ( 'NONE', 3,
 ( #15345, #1288, #25657, #23001, #33857, #4283 ),
 .UNSPECIFIED., .F., .F.,
 ( 4, 2, 4 ),
 ( 2.380729204623403261E-07, 0.003943479449179655878, 0.007886720825438849058 ),
 .UNSPECIFIED. ) ;
#7633=AXIS2_PLACEMENT_3D ( 'NONE', #20912, #23585, #7195 ) ;
#7726=CARTESIAN_POINT ( 'NONE',  ( 0.000000000000000000, 0.000000000000000000, 0.000000000000000000 ) ) ;
#7794=DIRECTION ( 'NONE',  ( 1.000000000000000000, 0.000000000000000000, -0.000000000000000000 ) ) ;
#7800=EDGE_LOOP ( 'NONE', ( #5558, #29761, #17522, #34106, #21177, #704 ) ) ;
#7828=CARTESIAN_POINT ( 'NONE',  ( 0.000000000000000000, -11.69134295108991672, -6.750000000000007105 ) ) ;
#7830=PLANE ( 'NONE',  #17526 ) ;
#7839=PLANE ( 'NONE',  #27929 ) ;
#7900=EDGE_CURVE ( 'NONE', #18455, #11327, #23813, .T. ) ;
#7933=EDGE_CURVE ( 'NONE', #32587, #8985, #20264, .T. ) ;
#8004=CARTESIAN_POINT ( 'NONE',  ( 0.1387913946425842759, -13.01149508916977204, -4.463429423125060858 ) ) ;
#8042=FACE_OUTER_BOUND ( 'NONE', #20726, .T. ) ;
#8112=ORIENTED_EDGE ( 'NONE', *, *, #34759, .F. ) ;
#8115=CARTESIAN_POINT ( 'NONE',  ( 0.1149164202474876467, -10.37169118567827653, -9.035703905990969176 ) ) ;
#8123=DIRECTION ( 'NONE',  ( -1.000000000000000000, 0.000000000000000000, -0.000000000000000000 ) ) ;
#8337=CARTESIAN_POINT ( 'NONE',  ( 55.00000000000000711, 0.000000000000000000, 0.000000000000000000 ) ) ;
#8482=CIRCLE ( 'NONE', #14192, 13.49999999999999822 ) ;
#8520=DIRECTION ( 'NONE',  ( -1.000000000000000000, -0.000000000000000000, -0.000000000000000000 ) ) ;
#8564=CARTESIAN_POINT ( 'NONE',  ( 0.000000000000000000, 0.000000000000000000, 0.000000000000000000 ) ) ;
#8643=EDGE_CURVE ( 'NONE', #32317, #10400, #13204, .T. ) ;
#8672=SHAPE_REPRESENTATION ( 'hex structural bolt gradec short_iso_ISO 7412 - M16 x 45 --- 26-WN', ( #28566 ), #29141 ) ;
#8697=ORIENTED_EDGE ( 'NONE', *, *, #34759, .T. ) ;
#8942=ORIENTED_EDGE ( 'NONE', *, *, #11091, .T. ) ;
#8985=VERTEX_POINT ( 'NONE', #5710 ) ;
#8987=DIRECTION ( 'NONE',  ( 0.000000000000000000, 0.000000000000000000, -1.000000000000000000 ) ) ;
#9042=VERTEX_POINT ( 'NONE', #1102 ) ;
#9156=STYLED_ITEM('',(#35282),#33646);
#9173=CARTESIAN_POINT ( 'NONE',  ( 9.199999999999999289, 11.69134295108991317, -6.750000000000016875 ) ) ;
#9235=CARTESIAN_POINT ( 'NONE',  ( 55.00000000000000711, 0.000000000000000000, 0.000000000000000000 ) ) ;
#9247=ADVANCED_FACE ( 'NONE', ( #32219 ), #7830, .F. ) ;
#9394=DIRECTION ( 'NONE',  ( 0.000000000000000000, 0.000000000000000000, 1.000000000000000000 ) ) ;
#9499=AXIS2_PLACEMENT_3D ( 'NONE', #6027, #19583, #33088 ) ;
#9506=CIRCLE ( 'NONE', #15844, 8.000000000000000000 ) ;
#9551=CARTESIAN_POINT ( 'NONE',  ( 0.000000000000000000, -11.69134295108990607, 6.750000000000024869 ) ) ;
#9589=CONICAL_SURFACE ( 'NONE', #15263, 6.898500000000000298, 0.7853981633974428389 ) ;
#9671=CARTESIAN_POINT ( 'NONE',  ( 0.02849990174189795042, 12.35429686688392259, 5.601730134768050817 ) ) ;
#9683=DIRECTION ( 'NONE',  ( -1.000000000000000000, -0.000000000000000000, -0.000000000000000000 ) ) ;
#9695=DIRECTION ( 'NONE',  ( -1.000000000000000000, -0.000000000000000000, -0.000000000000000000 ) ) ;
#9710=AXIS2_PLACEMENT_3D ( 'NONE', #20937, #1715, #34460 ) ;
#9711=CIRCLE ( 'NONE', #30190, 13.50000000000000178 ) ;
#9721=DIRECTION ( 'NONE',  ( -0.000000000000000000, 0.000000000000000000, -1.000000000000000000 ) ) ;
#9770=EDGE_CURVE ( 'NONE', #14536, #3150, #25275, .T. ) ;
#9786=B_SPLINE_CURVE_WITH_KNOTS ( 'NONE', 3,
 ( #9551, #12236, #26255, #4525, #23254, #20410, #25734, #31253 ),
 .UNSPECIFIED., .F., .F.,
 ( 4, 2, 2, 4 ),
 ( 0.007886720825438849058, 0.009850969036564048015, 0.01181521724768924697, 0.01574371366993964488 ),
 .UNSPECIFIED. ) ;
#9859=ORIENTED_EDGE ( 'NONE', *, *, #14620, .T. ) ;
#9873=CONICAL_SURFACE ( 'NONE', #20127, 13.50000000000000000, 1.047197551196600296 ) ;
#9888=VECTOR ( 'NONE', #29343, 1000.000000000000114 ) ;
#9914=ORIENTED_EDGE ( 'NONE', *, *, #6208, .F. ) ;
#10093=AXIS2_PLACEMENT_3D ( 'NONE', #1056, #33266, #6021 ) ;
#10204=DIRECTION ( 'NONE',  ( -1.000000000000000000, -0.000000000000000000, -0.000000000000000000 ) ) ;
#10257=VECTOR ( 'NONE', #15978, 1000.000000000000000 ) ;
#10334=PLANE ( 'NONE',  #4811 ) ;
#10371=EDGE_CURVE ( 'NONE', #32902, #33119, #33029, .T. ) ;
#10379=CARTESIAN_POINT ( 'NONE',  ( 55.00000000000000711, 0.000000000000000000, 0.000000000000000000 ) ) ;
#10400=VERTEX_POINT ( 'NONE', #27158 ) ;
#10407=CARTESIAN_POINT ( 'NONE',  ( 55.00000000000000711, 0.000000000000000000, 0.000000000000000000 ) ) ;
#10469=CARTESIAN_POINT ( 'NONE',  ( 0.000000000000000000, 9.797174393178825657E-16, -8.000000000000000000 ) ) ;
#10500=CARTESIAN_POINT ( 'NONE',  ( 1.205771365940040196, 7.794228634059932048, -13.49999999999999822 ) ) ;
#10531=ADVANCED_FACE ( 'NONE', ( #28042 ), #6138, .F. ) ;
#10536=SHAPE_REPRESENTATION_RELATIONSHIP ( 'NONE' , 'NONE' ,  #8672, #15210 ) ;
#10544=AXIS2_PLACEMENT_3D ( 'NONE', #29501, #26818, #32498 ) ;
#10563=LINE ( 'NONE', #16265, #19509 ) ;
#10586=AXIS2_PLACEMENT_3D ( 'NONE', #21893, #10702, #29385 ) ;
#10678=DIRECTION ( 'NONE',  ( 0.000000000000000000, 0.000000000000000000, -1.000000000000000000 ) ) ;
#10702=DIRECTION ( 'NONE',  ( -1.000000000000000000, -0.000000000000000000, -0.000000000000000000 ) ) ;
#10724=ORIENTED_EDGE ( 'NONE', *, *, #21845, .F. ) ;
#10775=CARTESIAN_POINT ( 'NONE',  ( 10.00000000000000000, -15.58845726811992627, 0.000000000000000000 ) ) ;
#10809=DIRECTION ( 'NONE',  ( -0.000000000000000000, 0.000000000000000000, 1.000000000000000000 ) ) ;
#10818=CARTESIAN_POINT ( 'NONE',  ( 0.8418677244542628335, 6.533629441834533758, -13.49999999999999822 ) ) ;
#11010=EDGE_CURVE ( 'NONE', #20439, #32701, #9506, .T. ) ;
#11053=( NAMED_UNIT ( * ) PLANE_ANGLE_UNIT ( ) SI_UNIT ( $, .RADIAN. ) );
#11089=DIRECTION ( 'NONE',  ( -1.000000000000000000, -0.000000000000000000, -0.000000000000000000 ) ) ;
#11091=EDGE_CURVE ( 'NONE', #11327, #32902, #32898, .T. ) ;
#11093=EDGE_CURVE ( 'NONE', #35009, #31908, #5657, .T. ) ;
#11268=CARTESIAN_POINT ( 'NONE',  ( 0.000000000000000000, -11.69134295108991672, -6.750000000000007105 ) ) ;
#11327=VERTEX_POINT ( 'NONE', #23119 ) ;
#11422=CARTESIAN_POINT ( 'NONE',  ( 0.000000000000000000, 0.000000000000000000, 0.000000000000000000 ) ) ;
#11490=PRODUCT_DEFINITION_SHAPE ( 'NONE', 'NONE',  #27721 ) ;
#11562=EDGE_LOOP ( 'NONE', ( #18081, #26384, #19547 ) ) ;
#11660=AXIS2_PLACEMENT_3D ( 'NONE', #2815, #155, #22579 ) ;
#11685=ORIENTED_EDGE ( 'NONE', *, *, #31018, .F. ) ;
#11698=CARTESIAN_POINT ( 'NONE',  ( 9.199999999999999289, 7.794228634059932048, -13.49999999999999822 ) ) ;
#11703=LINE ( 'NONE', #25382, #31353 ) ;
#11730=CARTESIAN_POINT ( 'NONE',  ( 1.205771365940041528, 7.794228634059941818, 13.49999999999999645 ) ) ;
#11778=ORIENTED_EDGE ( 'NONE', *, *, #114, .F. ) ;
#11784=CARTESIAN_POINT ( 'NONE',  ( 0.000000000000000000, 0.000000000000000000, -13.49999999999999822 ) ) ;
#11792=FACE_OUTER_BOUND ( 'NONE', #16310, .T. ) ;
#11805=CIRCLE ( 'NONE', #7217, 13.50000000000000000 ) ;
#11841=DIRECTION ( 'NONE',  ( -0.000000000000000000, 0.5000000000000012212, 0.8660254037844380415 ) ) ;
#11894=ORIENTED_EDGE ( 'NONE', *, *, #11093, .F. ) ;
#11959=ORIENTED_EDGE ( 'NONE', *, *, #458, .T. ) ;
#12173=EDGE_CURVE ( 'NONE', #34333, #13531, #2519, .T. ) ;
#12221=AXIS2_PLACEMENT_3D ( 'NONE', #5896, #11089, #33322 ) ;
#12236=CARTESIAN_POINT ( 'NONE',  ( -2.988332237913170807E-15, -11.36060796471277357, 7.322849800245833762 ) ) ;
#12253=CIRCLE ( 'NONE', #32114, 6.898500000000000298 ) ;
#12270=CARTESIAN_POINT ( 'NONE',  ( 9.199999999999999289, 13.50000000000000178, 0.000000000000000000 ) ) ;
#12356=DIRECTION ( 'NONE',  ( 1.000000000000000000, 0.000000000000000000, -0.000000000000000000 ) ) ;
#12418=ADVANCED_FACE ( 'NONE', ( #3711 ), #9589, .T. ) ;
#12440=VECTOR ( 'NONE', #8520, 1000.000000000000000 ) ;
#12514=DIRECTION ( 'NONE',  ( 0.000000000000000000, 0.000000000000000000, 1.000000000000000000 ) ) ;
#12524=PLANE ( 'NONE',  #19194 ) ;
#12566=VERTEX_POINT ( 'NONE', #19355 ) ;
#12613=CARTESIAN_POINT ( 'NONE',  ( 0.000000000000000000, 0.000000000000000000, 0.000000000000000000 ) ) ;
#12629=FACE_OUTER_BOUND ( 'NONE', #19329, .T. ) ;
#12722=CARTESIAN_POINT ( 'NONE',  ( 0.02849990174189666672, 11.02838903529590198, -7.898269865231970499 ) ) ;
#12727=ORIENTED_EDGE ( 'NONE', *, *, #9770, .T. ) ;
#12786=ORIENTED_EDGE ( 'NONE', *, *, #33046, .T. ) ;
#12820=B_SPLINE_CURVE_WITH_KNOTS ( 'NONE', 3,
 ( #34599, #29258, #12722, #18594, #15561, #15388, #26223, #23387 ),
 .UNSPECIFIED., .F., .F.,
 ( 4, 2, 2, 4 ),
 ( 0.007886720825438824772, 0.009850969036564027198, 0.01181521724768923136, 0.01574371366993963794 ),
 .UNSPECIFIED. ) ;
#12842=EDGE_CURVE ( 'NONE', #17480, #13509, #9786, .T. ) ;
#12973=CARTESIAN_POINT ( 'NONE',  ( 0.1134162231553477451, -2.627030748436328889, -13.50000000000000000 ) ) ;
#12984=EDGE_LOOP ( 'NONE', ( #20355, #27528, #30670 ) ) ;
#13029=CONICAL_SURFACE ( 'NONE', #32901, 13.50000000000000000, 1.047197551196600296 ) ;
#13073=DIRECTION ( 'NONE',  ( 1.000000000000000000, 0.000000000000000000, 0.000000000000000000 ) ) ;
#13075=ADVANCED_FACE ( 'NONE', ( #21790 ), #21900, .F. ) ;
#13076=EDGE_CURVE ( 'NONE', #33119, #5849, #8482, .T. ) ;
#13155=AXIS2_PLACEMENT_3D ( 'NONE', #32652, #27312, #274 ) ;
#13204=B_SPLINE_CURVE_WITH_KNOTS ( 'NONE', 3,
 ( #30862, #20369, #9671, #4143, #14861, #3799, #6467, #31559 ),
 .UNSPECIFIED., .F., .F.,
 ( 4, 2, 2, 4 ),
 ( 0.007886720825438786608, 0.009850969036563997708, 0.01181521724768920881, 0.01574371366993962754 ),
 .UNSPECIFIED. ) ;
#13216=DIRECTION ( 'NONE',  ( -1.000000000000000000, -0.000000000000000000, -0.000000000000000000 ) ) ;
#13321=DIRECTION ( 'NONE',  ( -1.000000000000000000, -0.000000000000000000, -0.000000000000000000 ) ) ;
#13355=DIRECTION ( 'NONE',  ( -1.000000000000000000, -0.000000000000000000, -0.000000000000000000 ) ) ;
#13411=CARTESIAN_POINT ( 'NONE',  ( 0.000000000000000000, 3.004629197474321612E-15, 13.50000000000000000 ) ) ;
#13422=ORIENTED_EDGE ( 'NONE', *, *, #31452, .T. ) ;
#13429=DIRECTION ( 'NONE',  ( -1.000000000000000000, -0.000000000000000000, -0.000000000000000000 ) ) ;
#13458=DIRECTION ( 'NONE',  ( 0.000000000000000000, 1.000000000000000000, -2.225651257388386197E-16 ) ) ;
#13490=EDGE_LOOP ( 'NONE', ( #27023, #14891, #23412, #861 ) ) ;
#13509=VERTEX_POINT ( 'NONE', #17957 ) ;
#13521=CARTESIAN_POINT ( 'NONE',  ( 9.199999999999999289, 15.58845726811990495, 0.000000000000000000 ) ) ;
#13523=LINE ( 'NONE', #24523, #34968 ) ;
#13531=VERTEX_POINT ( 'NONE', #7574 ) ;
#13613=CARTESIAN_POINT ( 'NONE',  ( 0.000000000000000000, 0.000000000000000000, 0.000000000000000000 ) ) ;
#13657=CARTESIAN_POINT ( 'NONE',  ( -9.359714067160018747E-16, 0.6596962799436644209, -13.49999999999999822 ) ) ;
#13677=ORIENTED_EDGE ( 'NONE', *, *, #21203, .T. ) ;
#13843=ORIENTED_EDGE ( 'NONE', *, *, #5915, .F. ) ;
#13893=DIRECTION ( 'NONE',  ( 1.000000000000000000, 0.000000000000000000, 0.000000000000000000 ) ) ;
#13900=ORIENTED_EDGE ( 'NONE', *, *, #20470, .T. ) ;
#13911=CONICAL_SURFACE ( 'NONE', #11660, 13.50000000000000000, 1.047197551196600296 ) ;
#13956=ORIENTED_EDGE ( 'NONE', *, *, #21511, .F. ) ;
#13983=DIRECTION ( 'NONE',  ( 0.000000000000000000, 0.000000000000000000, -1.000000000000000000 ) ) ;
#14009=CARTESIAN_POINT ( 'NONE',  ( 55.00000000000000711, 0.000000000000000000, 0.000000000000000000 ) ) ;
#14022=ORIENTED_EDGE ( 'NONE', *, *, #27763, .F. ) ;
#14114=CARTESIAN_POINT ( 'NONE',  ( 0.2222207399958900931, 3.306033584716338236, 13.49999999999999645 ) ) ;
#14192=AXIS2_PLACEMENT_3D ( 'NONE', #13613, #19145, #29985 ) ;
#14283=VERTEX_POINT ( 'NONE', #11730 ) ;
#14414=DIRECTION ( 'NONE',  ( 0.000000000000000000, 0.000000000000000000, -1.000000000000000000 ) ) ;
#14536=VERTEX_POINT ( 'NONE', #1901 ) ;
#14537=ORIENTED_EDGE ( 'NONE', *, *, #23306, .F. ) ;
#14590=DIRECTION ( 'NONE',  ( 1.000000000000000000, 0.000000000000000000, 0.000000000000000000 ) ) ;
#14620=EDGE_CURVE ( 'NONE', #9042, #3150, #5784, .T. ) ;
#14645=FACE_OUTER_BOUND ( 'NONE', #17979, .T. ) ;
#14700=ORIENTED_EDGE ( 'NONE', *, *, #670, .F. ) ;
#14744=CIRCLE ( 'NONE', #26659, 13.50000000000000178 ) ;
#14759=ORIENTED_EDGE ( 'NONE', *, *, #7401, .T. ) ;
#14861=CARTESIAN_POINT ( 'NONE',  ( 0.2204769333330968695, 13.33789614101571885, 3.898086217683919941 ) ) ;
#14865=CARTESIAN_POINT ( 'NONE',  ( 1.205771365940050854, -7.794228634059966687, -13.49999999999999822 ) ) ;
#14878=AXIS2_PLACEMENT_3D ( 'NONE', #12270, #14590, #28093 ) ;
#14891=ORIENTED_EDGE ( 'NONE', *, *, #114, .T. ) ;
#14979=EDGE_LOOP ( 'NONE', ( #14537, #6623, #5546, #10724, #13900, #27893 ) ) ;
#15021=LINE ( 'NONE', #28190, #32436 ) ;
#15052=VECTOR ( 'NONE', #29966, 1000.000000000000000 ) ;
#15084=FACE_OUTER_BOUND ( 'NONE', #14979, .T. ) ;
#15173=AXIS2_PLACEMENT_3D ( 'NONE', #25470, #19449, #27792 ) ;
#15210=ADVANCED_BREP_SHAPE_REPRESENTATION ( '', ( #33646, #28566 ), #29141 ) ;
#15259=DIRECTION ( 'NONE',  ( 1.000000000000000000, 0.000000000000000000, -0.000000000000000000 ) ) ;
#15263=AXIS2_PLACEMENT_3D ( 'NONE', #9235, #6377, #212 ) ;
#15270=ORIENTED_EDGE ( 'NONE', *, *, #21845, .T. ) ;
#15345=CARTESIAN_POINT ( 'NONE',  ( 1.205771365940061957, -15.58845726811992449, 7.826847450972439323E-16 ) ) ;
#15388=CARTESIAN_POINT ( 'NONE',  ( 0.5355294694855705639, 9.071383756617057870, -11.28790243858421327 ) ) ;
#15478=EDGE_CURVE ( 'NONE', #20728, #32317, #7442, .T. ) ;
#15561=CARTESIAN_POINT ( 'NONE',  ( 0.2204769333330932612, 10.04478976116410927, -9.601913782316097823 ) ) ;
#15570=VERTEX_POINT ( 'NONE', #31125 ) ;
#15591=AXIS2_PLACEMENT_3D ( 'NONE', #17554, #3809, #8987 ) ;
#15605=ADVANCED_FACE ( 'NONE', ( #17784 ), #25770, .T. ) ;
#15606=( NAMED_UNIT ( * ) SI_UNIT ( $, .STERADIAN. ) SOLID_ANGLE_UNIT ( ) );
#15660=DIRECTION ( 'NONE',  ( 0.000000000000000000, 1.000000000000000000, -0.000000000000000000 ) ) ;
#15673=ORIENTED_EDGE ( 'NONE', *, *, #33046, .F. ) ;
#15722=ORIENTED_EDGE ( 'NONE', *, *, #12842, .T. ) ;
#15760=ADVANCED_FACE ( 'NONE', ( #1908 ), #27002, .F. ) ;
#15822=DIRECTION ( 'NONE',  ( -1.000000000000000000, -0.000000000000000000, -0.000000000000000000 ) ) ;
#15844=AXIS2_PLACEMENT_3D ( 'NONE', #35063, #26859, #10678 ) ;
#15860=EDGE_LOOP ( 'NONE', ( #1465, #21697, #25385, #21208, #14700, #647 ) ) ;
#15873=ORIENTED_EDGE ( 'NONE', *, *, #1370, .T. ) ;
#15893=ORIENTED_EDGE ( 'NONE', *, *, #26629, .T. ) ;
#15947=DIRECTION ( 'NONE',  ( 0.000000000000000000, -0.5000000000000018874, -0.8660254037844374864 ) ) ;
#15967=DIRECTION ( 'NONE',  ( 0.000000000000000000, -2.225651257388386197E-16, -1.000000000000000000 ) ) ;
#15978=DIRECTION ( 'NONE',  ( 0.000000000000000000, -1.000000000000000000, 2.225651257388386197E-16 ) ) ;
#16059=UNCERTAINTY_MEASURE_WITH_UNIT (LENGTH_MEASURE( 1.000000000000000082E-05 ), #29921, 'distance_accuracy_value', 'NONE');
#16139=EDGE_CURVE ( 'NONE', #17480, #33119, #17139, .T. ) ;
#16200=CARTESIAN_POINT ( 'NONE',  ( 10.00000000000000000, -7.794228634059966687, -13.49999999999999822 ) ) ;
#16244=ADVANCED_FACE ( 'NONE', ( #2220 ), #30739, .T. ) ;
#16265=CARTESIAN_POINT ( 'NONE',  ( 10.00000000000000000, -7.794228634059937377, 13.50000000000000000 ) ) ;
#16293=EDGE_CURVE ( 'NONE', #12566, #27067, #5053, .T. ) ;
#16310=EDGE_LOOP ( 'NONE', ( #26834, #4957, #25314, #7054 ) ) ;
#16348=DIRECTION ( 'NONE',  ( 0.000000000000000000, 0.5000000000000004441, -0.8660254037844382635 ) ) ;
#16351=CARTESIAN_POINT ( 'NONE',  ( 0.1396634953578575200, 2.649662288468964011, -13.49999999999999822 ) ) ;
#16391=EDGE_LOOP ( 'NONE', ( #19337, #30993, #475 ) ) ;
#16470=CARTESIAN_POINT ( 'NONE',  ( 9.199999999999999289, -15.58845726811992627, 0.000000000000000000 ) ) ;
#16764=DIRECTION ( 'NONE',  ( -1.000000000000000000, -0.000000000000000000, -0.000000000000000000 ) ) ;
#16777=CARTESIAN_POINT ( 'NONE',  ( 9.199999999999999289, 15.58845726811990495, 0.000000000000000000 ) ) ;
#16820=ADVANCED_FACE ( 'NONE', ( #19625 ), #9873, .T. ) ;
#16845=ADVANCED_FACE ( 'NONE', ( #11792 ), #32944, .T. ) ;
#16862=DIRECTION ( 'NONE',  ( 0.000000000000000000, -0.5000000000000004441, 0.8660254037844382635 ) ) ;
#16911=CARTESIAN_POINT ( 'NONE',  ( 0.000000000000000000, 0.000000000000000000, 0.000000000000000000 ) ) ;
#16916=ORIENTED_EDGE ( 'NONE', *, *, #33742, .T. ) ;
#16951=SHAPE_DEFINITION_REPRESENTATION ( #11490, #8672 ) ;
#17139=CIRCLE ( 'NONE', #18248, 13.49999999999999822 ) ;
#17146=CARTESIAN_POINT ( 'NONE',  ( 0.000000000000000000, 3.004629197474321612E-15, 13.50000000000000000 ) ) ;
#17174=B_SPLINE_CURVE_WITH_KNOTS ( 'NONE', 3,
 ( #4618, #31522, #23513, #7300, #26010, #20675 ),
 .UNSPECIFIED., .F., .F.,
 ( 4, 2, 4 ),
 ( 2.380729204601676866E-07, 0.003943479449179642000, 0.007886720825438824772 ),
 .UNSPECIFIED. ) ;
#17413=VECTOR ( 'NONE', #11841, 999.9999999999998863 ) ;
#17480=VERTEX_POINT ( 'NONE', #19874 ) ;
#17500=EDGE_LOOP ( 'NONE', ( #19619, #26027, #12727, #105, #17920, #15673 ) ) ;
#17522=ORIENTED_EDGE ( 'NONE', *, *, #1370, .F. ) ;
#17526=AXIS2_PLACEMENT_3D ( 'NONE', #18716, #29556, #7120 ) ;
#17554=CARTESIAN_POINT ( 'NONE',  ( 0.000000000000000000, 0.000000000000000000, 0.000000000000000000 ) ) ;
#17566=DIRECTION ( 'NONE',  ( 0.000000000000000000, 0.000000000000000000, 1.000000000000000000 ) ) ;
#17653=ADVANCED_FACE ( 'NONE', ( #26070 ), #25722, .T. ) ;
#17784=FACE_OUTER_BOUND ( 'NONE', #25775, .T. ) ;
#17794=VERTEX_POINT ( 'NONE', #9173 ) ;
#17835=PLANE ( 'NONE',  #2653 ) ;
#17876=EDGE_CURVE ( 'NONE', #9042, #14283, #2553, .T. ) ;
#17920=ORIENTED_EDGE ( 'NONE', *, *, #33789, .F. ) ;
#17957=CARTESIAN_POINT ( 'NONE',  ( 1.205771365940041306, -7.794228634059936489, 13.50000000000000000 ) ) ;
#17979=EDGE_LOOP ( 'NONE', ( #2721, #505, #11959 ) ) ;
#17997=EDGE_CURVE ( 'NONE', #8985, #32701, #21959, .T. ) ;
#18024=CARTESIAN_POINT ( 'NONE',  ( 10.00000000000000000, 0.000000000000000000, 8.000000000000000000 ) ) ;
#18037=EDGE_LOOP ( 'NONE', ( #8112, #8942, #19917, #28588, #4687, #23830 ) ) ;
#18081=ORIENTED_EDGE ( 'NONE', *, *, #34320, .T. ) ;
#18218=CARTESIAN_POINT ( 'NONE',  ( 10.00000000000000000, 7.794228634059932048, -13.49999999999999822 ) ) ;
#18248=AXIS2_PLACEMENT_3D ( 'NONE', #1532, #29099, #26081 ) ;
#18324=CARTESIAN_POINT ( 'NONE',  ( 0.000000000000000000, 0.000000000000000000, -13.49999999999999822 ) ) ;
#18455=VERTEX_POINT ( 'NONE', #33114 ) ;
#18501=EDGE_CURVE ( 'NONE', #3150, #23862, #2857, .T. ) ;
#18505=CARTESIAN_POINT ( 'NONE',  ( 1.205771365940050854, -7.794228634059966687, -13.49999999999999822 ) ) ;
#18594=CARTESIAN_POINT ( 'NONE',  ( 0.1387913946425707035, 10.37119081301007739, -9.036570576874957794 ) ) ;
#18632=DIRECTION ( 'NONE',  ( 0.000000000000000000, 0.000000000000000000, 1.000000000000000000 ) ) ;
#18639=FACE_OUTER_BOUND ( 'NONE', #19230, .T. ) ;
#18679=CIRCLE ( 'NONE', #29484, 13.50000000000000178 ) ;
#18716=CARTESIAN_POINT ( 'NONE',  ( 10.00000000000000000, 7.794228634059932048, -13.49999999999999822 ) ) ;
#18734=ADVANCED_FACE ( 'NONE', ( #7103 ), #5613, .T. ) ;
#18786=ORIENTED_EDGE ( 'NONE', *, *, #19452, .T. ) ;
#18817=CARTESIAN_POINT ( 'NONE',  ( 0.8377008405913533018, -8.431745484732017459, -12.39578842395470559 ) ) ;
#18860=AXIS2_PLACEMENT_3D ( 'NONE', #16911, #30942, #14414 ) ;
#18872=ORIENTED_EDGE ( 'NONE', *, *, #30371, .T. ) ;
#18882=CARTESIAN_POINT ( 'NONE',  ( 1.205771365940061957, -15.58845726811992449, 7.826847450972439323E-16 ) ) ;
#18994=CARTESIAN_POINT ( 'NONE',  ( 3.754050022231059103E-15, -11.02739026146942969, -7.899999792244740249 ) ) ;
#19055=VECTOR ( 'NONE', #27365, 1000.000000000000000 ) ;
#19145=DIRECTION ( 'NONE',  ( 1.000000000000000000, 0.000000000000000000, -0.000000000000000000 ) ) ;
#19194=AXIS2_PLACEMENT_3D ( 'NONE', #25511, #12356, #34405 ) ;
#19230=EDGE_LOOP ( 'NONE', ( #31587, #31860, #33636, #7587, #27660, #28816 ) ) ;
#19260=ORIENTED_EDGE ( 'NONE', *, *, #33789, .T. ) ;
#19329=EDGE_LOOP ( 'NONE', ( #11894, #6270, #33336, #13956, #30846, #13843 ) ) ;
#19337=ORIENTED_EDGE ( 'NONE', *, *, #480, .T. ) ;
#19355=CARTESIAN_POINT ( 'NONE',  ( 9.199999999999999289, -11.69134295108990962, 6.750000000000026645 ) ) ;
#19361=ORIENTED_EDGE ( 'NONE', *, *, #11093, .T. ) ;
#19390=VERTEX_POINT ( 'NONE', #1480 ) ;
#19434=DIRECTION ( 'NONE',  ( 0.000000000000000000, -1.000000000000000000, 2.225651257388386197E-16 ) ) ;
#19449=DIRECTION ( 'NONE',  ( 1.000000000000000000, 0.000000000000000000, 0.000000000000000000 ) ) ;
#19452=EDGE_CURVE ( 'NONE', #13509, #32964, #7128, .T. ) ;
#19480=CIRCLE ( 'NONE', #1282, 8.000000000000000000 ) ;
#19509=VECTOR ( 'NONE', #29767, 1000.000000000000000 ) ;
#19547=ORIENTED_EDGE ( 'NONE', *, *, #31018, .T. ) ;
#19583=DIRECTION ( 'NONE',  ( 1.000000000000000000, 0.000000000000000000, -0.000000000000000000 ) ) ;
#19619=ORIENTED_EDGE ( 'NONE', *, *, #31471, .F. ) ;
#19625=FACE_OUTER_BOUND ( 'NONE', #16391, .T. ) ;
#19679=ORIENTED_EDGE ( 'NONE', *, *, #3853, .T. ) ;
#19747=AXIS2_PLACEMENT_3D ( 'NONE', #4837, #21047, #5364 ) ;
#19751=ORIENTED_EDGE ( 'NONE', *, *, #33928, .T. ) ;
#19874=CARTESIAN_POINT ( 'NONE',  ( 0.000000000000000000, -11.69134295108990607, 6.750000000000024869 ) ) ;
#19915=EDGE_LOOP ( 'NONE', ( #15873, #29340, #28858 ) ) ;
#19917=ORIENTED_EDGE ( 'NONE', *, *, #31452, .F. ) ;
#19970=CARTESIAN_POINT ( 'NONE',  ( 0.5344654698445916452, 9.073918974790291969, 11.28351131189991108 ) ) ;
#20079=CARTESIAN_POINT ( 'NONE',  ( 0.000000000000000000, 0.000000000000000000, 0.000000000000000000 ) ) ;
#20122=ORIENTED_EDGE ( 'NONE', *, *, #33928, .F. ) ;
#20127=AXIS2_PLACEMENT_3D ( 'NONE', #11422, #27787, #3755 ) ;
#20157=DIRECTION ( 'NONE',  ( 0.000000000000000000, 1.000000000000000000, -0.000000000000000000 ) ) ;
#20209=FACE_OUTER_BOUND ( 'NONE', #22239, .T. ) ;
#20244=DIRECTION ( 'NONE',  ( 0.000000000000000000, -0.5000000000000018874, -0.8660254037844374864 ) ) ;
#20264=CIRCLE ( 'NONE', #23107, 8.000000000000000000 ) ;
#20353=CARTESIAN_POINT ( 'NONE',  ( 9.199999999999999289, 0.000000000000000000, 13.50000000000000178 ) ) ;
#20355=ORIENTED_EDGE ( 'NONE', *, *, #8643, .T. ) ;
#20369=CARTESIAN_POINT ( 'NONE',  ( -7.920605089774962471E-15, 12.02207793746705455, 6.177150199754207094 ) ) ;
#20383=VECTOR ( 'NONE', #16764, 1000.000000000000000 ) ;
#20410=CARTESIAN_POINT ( 'NONE',  ( 0.5355294694855750048, -9.071383756617063199, 11.28790243858421505 ) ) ;
#20439=VERTEX_POINT ( 'NONE', #4563 ) ;
#20470=EDGE_CURVE ( 'NONE', #32964, #32317, #11805, .T. ) ;
#20675=CARTESIAN_POINT ( 'NONE',  ( 0.000000000000000000, 11.69134295108991140, -6.750000000000015987 ) ) ;
#20700=CARTESIAN_POINT ( 'NONE',  ( 1.205771365940041306, -7.794228634059936489, 13.50000000000000000 ) ) ;
#20726=EDGE_LOOP ( 'NONE', ( #14759, #19361, #16916 ) ) ;
#20728=VERTEX_POINT ( 'NONE', #25869 ) ;
#20771=ADVANCED_FACE ( 'NONE', ( #33701, #4139 ), #12524, .T. ) ;
#20784=VERTEX_POINT ( 'NONE', #6639 ) ;
#20912=CARTESIAN_POINT ( 'NONE',  ( 10.00000000000000000, 0.000000000000000000, 0.000000000000000000 ) ) ;
#20937=CARTESIAN_POINT ( 'NONE',  ( 0.000000000000000000, 0.000000000000000000, 0.000000000000000000 ) ) ;
#20949=EDGE_LOOP ( 'NONE', ( #27707, #24008, #20122, #25422 ) ) ;
#20968=ADVANCED_FACE ( 'NONE', ( #8042 ), #2182, .T. ) ;
#20972=LINE ( 'NONE', #10469, #30831 ) ;
#21047=DIRECTION ( 'NONE',  ( 1.000000000000000000, 0.000000000000000000, 0.000000000000000000 ) ) ;
#21111=PLANE ( 'NONE',  #7459 ) ;
#21148=LINE ( 'NONE', #31992, #4706 ) ;
#21177=ORIENTED_EDGE ( 'NONE', *, *, #29153, .F. ) ;
#21203=EDGE_CURVE ( 'NONE', #34376, #27996, #22046, .T. ) ;
#21208=ORIENTED_EDGE ( 'NONE', *, *, #33742, .F. ) ;
#21254=CARTESIAN_POINT ( 'NONE',  ( 10.00000000000000000, 7.794228634059941818, 13.49999999999999645 ) ) ;
#21378=DIRECTION ( 'NONE',  ( 1.000000000000000000, 0.000000000000000000, 0.000000000000000000 ) ) ;
#21434=CIRCLE ( 'NONE', #9499, 13.49999999999999822 ) ;
#21435=VECTOR ( 'NONE', #24355, 999.9999999999998863 ) ;
#21511=EDGE_CURVE ( 'NONE', #14283, #32317, #21811, .T. ) ;
#21531=ADVANCED_FACE ( 'NONE', ( #14645 ), #3230, .T. ) ;
#21665=CARTESIAN_POINT ( 'NONE',  ( 0.2222207399973191444, 3.306033584726114860, -13.49999999999999645 ) ) ;
#21692=ADVANCED_FACE ( 'NONE', ( #31337 ), #17835, .F. ) ;
#21697=ORIENTED_EDGE ( 'NONE', *, *, #31471, .T. ) ;
#21718=CARTESIAN_POINT ( 'NONE',  ( 9.199999999999999289, 13.50000000000000178, 0.000000000000000000 ) ) ;
#21790=FACE_OUTER_BOUND ( 'NONE', #5314, .T. ) ;
#21798=CONICAL_SURFACE ( 'NONE', #5296, 13.50000000000000000, 1.047197551196600296 ) ;
#21811=B_SPLINE_CURVE_WITH_KNOTS ( 'NONE', 3,
 ( #30651, #27616, #19970, #33840, #6065, #3924 ),
 .UNSPECIFIED., .F., .F.,
 ( 4, 2, 4 ),
 ( 2.380729204614569766E-07, 0.003943479449179625521, 0.007886720825438786608 ),
 .UNSPECIFIED. ) ;
#21833=DIRECTION ( 'NONE',  ( 0.000000000000000000, 0.000000000000000000, 1.000000000000000000 ) ) ;
#21843=CARTESIAN_POINT ( 'NONE',  ( 55.00000000000000711, 8.448225943918016683E-16, -6.898500000000000298 ) ) ;
#21845=EDGE_CURVE ( 'NONE', #32964, #17480, #21434, .T. ) ;
#21893=CARTESIAN_POINT ( 'NONE',  ( 9.199999999999999289, 0.000000000000000000, 0.000000000000000000 ) ) ;
#21900=PLANE ( 'NONE',  #29526 ) ;
#21959=LINE ( 'NONE', #30674, #15052 ) ;
#22035=CARTESIAN_POINT ( 'NONE',  ( 10.00000000000000000, -15.58845726811992627, 0.000000000000000000 ) ) ;
#22046=CIRCLE ( 'NONE', #6693, 6.898500000000000298 ) ;
#22093=CARTESIAN_POINT ( 'NONE',  ( 9.199999999999999289, 7.794228634059941818, 13.49999999999999645 ) ) ;
#22133=ORIENTED_EDGE ( 'NONE', *, *, #23466, .F. ) ;
#22206=CYLINDRICAL_SURFACE ( 'NONE', #33641, 13.50000000000000178 ) ;
#22237=FACE_OUTER_BOUND ( 'NONE', #15860, .T. ) ;
#22239=EDGE_LOOP ( 'NONE', ( #18786, #15270, #15722 ) ) ;
#22282=AXIS2_PLACEMENT_3D ( 'NONE', #14009, #8123, #10809 ) ;
#22303=ORIENTED_EDGE ( 'NONE', *, *, #34717, .T. ) ;
#22368=DIRECTION ( 'NONE',  ( -0.000000000000000000, 0.5000000000000012212, 0.8660254037844380415 ) ) ;
#22473=CARTESIAN_POINT ( 'NONE',  ( 0.8418677244547475569, 6.533629441836217744, 13.49999999999999645 ) ) ;
#22579=DIRECTION ( 'NONE',  ( 0.000000000000000000, 0.000000000000000000, -1.000000000000000000 ) ) ;
#22659=CARTESIAN_POINT ( 'NONE',  ( 9.199999999999999289, -15.58845726811992449, 0.000000000000000000 ) ) ;
#22715=ORIENTED_EDGE ( 'NONE', *, *, #11091, .F. ) ;
#22819=LINE ( 'NONE', #6073, #24744 ) ;
#22854=AXIS2_PLACEMENT_3D ( 'NONE', #24166, #7794, #35047 ) ;
#22870=DIRECTION ( 'NONE',  ( 0.000000000000000000, 0.000000000000000000, -1.000000000000000000 ) ) ;
#23001=CARTESIAN_POINT ( 'NONE',  ( 0.1149164202474821789, -13.01099471650158712, 4.464296094009060134 ) ) ;
#23006=AXIS2_PLACEMENT_3D ( 'NONE', #29596, #23732, #23891 ) ;
#23092=ADVANCED_FACE ( 'NONE', ( #12629 ), #23463, .F. ) ;
#23107=AXIS2_PLACEMENT_3D ( 'NONE', #2440, #13321, #21833 ) ;
#23119=CARTESIAN_POINT ( 'NONE',  ( 9.199999999999999289, -7.794228634059966687, -13.49999999999999822 ) ) ;
#23179=CARTESIAN_POINT ( 'NONE',  ( 9.199999999999999289, 7.794228634059932048, -13.49999999999999822 ) ) ;
#23200=CARTESIAN_POINT ( 'NONE',  ( 0.8394537150690343230, -6.525267068024321659, 13.49999999999999822 ) ) ;
#23254=CARTESIAN_POINT ( 'NONE',  ( 0.2204769333330994785, -10.04478976116411459, 9.601913782316108481 ) ) ;
#23264=( LENGTH_UNIT ( ) NAMED_UNIT ( * ) SI_UNIT ( .MILLI., .METRE. ) );
#23306=EDGE_CURVE ( 'NONE', #5849, #20728, #620, .T. ) ;
#23387=CARTESIAN_POINT ( 'NONE',  ( 1.205771365940040196, 7.794228634059932048, -13.49999999999999822 ) ) ;
#23412=ORIENTED_EDGE ( 'NONE', *, *, #6208, .T. ) ;
#23436=ORIENTED_EDGE ( 'NONE', *, *, #34320, .F. ) ;
#23463=PLANE ( 'NONE',  #34798 ) ;
#23466=EDGE_CURVE ( 'NONE', #27067, #18455, #26620, .T. ) ;
#23513=CARTESIAN_POINT ( 'NONE',  ( 0.5344654698445945318, 14.30876692738954858, -2.216488688100095139 ) ) ;
#23557=CARTESIAN_POINT ( 'NONE',  ( 0.000000000000000000, 11.69134295108991495, 6.750000000000012434 ) ) ;
#23585=DIRECTION ( 'NONE',  ( 1.000000000000000000, 0.000000000000000000, -0.000000000000000000 ) ) ;
#23637=DIRECTION ( 'NONE',  ( 0.000000000000000000, 0.000000000000000000, 1.000000000000000000 ) ) ;
#23732=DIRECTION ( 'NONE',  ( 1.000000000000000000, 0.000000000000000000, 0.000000000000000000 ) ) ;
#23745=EDGE_CURVE ( 'NONE', #10400, #20728, #17174, .T. ) ;
#23751=ORIENTED_EDGE ( 'NONE', *, *, #30371, .F. ) ;
#23813=LINE ( 'NONE', #129, #26495 ) ;
#23830=ORIENTED_EDGE ( 'NONE', *, *, #458, .F. ) ;
#23862=VERTEX_POINT ( 'NONE', #3020 ) ;
#23891=DIRECTION ( 'NONE',  ( 0.000000000000000000, 0.000000000000000000, -1.000000000000000000 ) ) ;
#23899=ADVANCED_FACE ( 'NONE', ( #5335 ), #7839, .T. ) ;
#23929=( GEOMETRIC_REPRESENTATION_CONTEXT ( 3 ) GLOBAL_UNCERTAINTY_ASSIGNED_CONTEXT ( ( #756 ) ) GLOBAL_UNIT_ASSIGNED_CONTEXT ( ( #23264, #4533, #15606 ) ) REPRESENTATION_CONTEXT ( 'NONE', 'WORKASPACE' ) );
#24008=ORIENTED_EDGE ( 'NONE', *, *, #24824, .T. ) ;
#24015=DIRECTION ( 'NONE',  ( 0.000000000000000000, -0.8660254037844380415, 0.5000000000000012212 ) ) ;
#24076=CIRCLE ( 'NONE', #237, 8.000000000000000000 ) ;
#24161=CLOSED_SHELL ( 'NONE', ( #5317, #12418, #17653, #20771, #16845, #16244, #15760, #21531, #20968, #33419, #18734, #23899, #15605, #24342, #33685, #4165, #16820, #26686, #33012, #32091, #2198, #9247, #10531, #13075, #28212, #23092, #21692 ) ) ;
#24166=CARTESIAN_POINT ( 'NONE',  ( 10.00000000000000000, 0.000000000000000000, 0.000000000000000000 ) ) ;
#24342=ADVANCED_FACE ( 'NONE', ( #3854 ), #22206, .T. ) ;
#24355=DIRECTION ( 'NONE',  ( 0.000000000000000000, -0.5000000000000008882, 0.8660254037844382635 ) ) ;
#24460=CARTESIAN_POINT ( 'NONE',  ( 10.00000000000000000, 7.794228634059941818, 13.49999999999999645 ) ) ;
#24523=CARTESIAN_POINT ( 'NONE',  ( 55.00000000000000711, 0.000000000000000000, 6.898500000000000298 ) ) ;
#24635=DIRECTION ( 'NONE',  ( -1.000000000000000000, -0.000000000000000000, -0.000000000000000000 ) ) ;
#24681=VECTOR ( 'NONE', #2177, 1000.000000000000000 ) ;
#24732=DIRECTION ( 'NONE',  ( 0.000000000000000000, 0.000000000000000000, -1.000000000000000000 ) ) ;
#24744=VECTOR ( 'NONE', #20157, 1000.000000000000000 ) ;
#24824=EDGE_CURVE ( 'NONE', #32587, #20439, #20972, .T. ) ;
#25046=EDGE_CURVE ( 'NONE', #13531, #5849, #25528, .T. ) ;
#25052=VECTOR ( 'NONE', #15947, 1000.000000000000114 ) ;
#25106=DIRECTION ( 'NONE',  ( 0.000000000000000000, 0.000000000000000000, 1.000000000000000000 ) ) ;
#25189=ORIENTED_EDGE ( 'NONE', *, *, #23466, .T. ) ;
#25220=PRODUCT_DEFINITION_FORMATION_WITH_SPECIFIED_SOURCE ( 'ANY', '', #32778, .NOT_KNOWN. ) ;
#25275=LINE ( 'NONE', #3741, #20383 ) ;
#25314=ORIENTED_EDGE ( 'NONE', *, *, #17997, .T. ) ;
#25350=CARTESIAN_POINT ( 'NONE',  ( 10.00000000000000000, 0.000000000000000000, 0.000000000000000000 ) ) ;
#25382=CARTESIAN_POINT ( 'NONE',  ( 9.199999999999999289, -15.58845726811992627, 0.000000000000000000 ) ) ;
#25385=ORIENTED_EDGE ( 'NONE', *, *, #3408, .F. ) ;
#25422=ORIENTED_EDGE ( 'NONE', *, *, #17997, .F. ) ;
#25426=CYLINDRICAL_SURFACE ( 'NONE', #10093, 13.50000000000000178 ) ;
#25470=CARTESIAN_POINT ( 'NONE',  ( 9.199999999999999289, 13.50000000000000178, 0.000000000000000000 ) ) ;
#25511=CARTESIAN_POINT ( 'NONE',  ( 10.00000000000000000, 15.58845726811990673, -2.400813222210650817E-15 ) ) ;
#25528=B_SPLINE_CURVE_WITH_KNOTS ( 'NONE', 3,
 ( #10500, #10818, #5799, #21665, #16351, #27181, #13657, #1018 ),
 .UNSPECIFIED., .F., .F.,
 ( 4, 2, 2, 4 ),
 ( 0.03601148258275851249, 0.03996050705323227203, 0.04193501928846914834, 0.04390953152370602464 ),
 .UNSPECIFIED. ) ;
#25657=CARTESIAN_POINT ( 'NONE',  ( 0.5344654698446028585, -14.30876692738956457, 2.216488688100102689 ) ) ;
#25722=CYLINDRICAL_SURFACE ( 'NONE', #25803, 8.000000000000000000 ) ;
#25734=CARTESIAN_POINT ( 'NONE',  ( 0.8386200322165722199, -8.430153398135434628, 12.39854599882999864 ) ) ;
#25737=EDGE_CURVE ( 'NONE', #23862, #13509, #10563, .T. ) ;
#25770=PLANE ( 'NONE',  #14878 ) ;
#25775=EDGE_LOOP ( 'NONE', ( #4565, #8697, #12786 ) ) ;
#25803=AXIS2_PLACEMENT_3D ( 'NONE', #1347, #9695, #17566 ) ;
#25847=EDGE_LOOP ( 'NONE', ( #22133, #2839, #11685, #29044, #22715, #5343 ) ) ;
#25865=DIRECTION ( 'NONE',  ( -1.000000000000000000, -0.000000000000000000, -0.000000000000000000 ) ) ;
#25869=CARTESIAN_POINT ( 'NONE',  ( 0.000000000000000000, 11.69134295108991140, -6.750000000000015987 ) ) ;
#25884=ORIENTED_EDGE ( 'NONE', *, *, #16293, .T. ) ;
#26010=CARTESIAN_POINT ( 'NONE',  ( -1.035074261544755014E-14, 12.35529564071042330, -5.600000207755282844 ) ) ;
#26027=ORIENTED_EDGE ( 'NONE', *, *, #34717, .F. ) ;
#26070=FACE_OUTER_BOUND ( 'NONE', #20949, .T. ) ;
#26081=DIRECTION ( 'NONE',  ( 0.000000000000000000, 0.000000000000000000, -1.000000000000000000 ) ) ;
#26223=CARTESIAN_POINT ( 'NONE',  ( 0.8386200322165693333, 8.430153398135427523, -12.39854599882999509 ) ) ;
#26255=CARTESIAN_POINT ( 'NONE',  ( 0.02849990174190264458, -11.02838903529590198, 7.898269865231986486 ) ) ;
#26384=ORIENTED_EDGE ( 'NONE', *, *, #16139, .T. ) ;
#26485=CARTESIAN_POINT ( 'NONE',  ( -1.105377996166861548E-15, -1.318430554028759305, -13.49999999999999645 ) ) ;
#26494=LINE ( 'NONE', #34685, #2378 ) ;
#26495=VECTOR ( 'NONE', #16348, 1000.000000000000227 ) ;
#26579=CARTESIAN_POINT ( 'NONE',  ( 0.000000000000000000, 0.000000000000000000, 0.000000000000000000 ) ) ;
#26620=LINE ( 'NONE', #95, #29033 ) ;
#26629=EDGE_CURVE ( 'NONE', #27996, #32587, #5111, .T. ) ;
#26659=AXIS2_PLACEMENT_3D ( 'NONE', #4595, #13355, #5312 ) ;
#26671=ORIENTED_EDGE ( 'NONE', *, *, #11010, .T. ) ;
#26686=ADVANCED_FACE ( 'NONE', ( #20209 ), #4208, .T. ) ;
#26715=EDGE_CURVE ( 'NONE', #8985, #32587, #24076, .T. ) ;
#26778=DIRECTION ( 'NONE',  ( 0.000000000000000000, 0.5000000000000018874, 0.8660254037844374864 ) ) ;
#26818=DIRECTION ( 'NONE',  ( 1.000000000000000000, 0.000000000000000000, 0.000000000000000000 ) ) ;
#26834=ORIENTED_EDGE ( 'NONE', *, *, #24824, .F. ) ;
#26859=DIRECTION ( 'NONE',  ( -1.000000000000000000, -0.000000000000000000, 0.000000000000000000 ) ) ;
#26873=CARTESIAN_POINT ( 'NONE',  ( 0.2204769333331085268, -13.33789614101574372, -3.898086217683921273 ) ) ;
#26975=VECTOR ( 'NONE', #13429, 1000.000000000000000 ) ;
#27002=PLANE ( 'NONE',  #22282 ) ;
#27023=ORIENTED_EDGE ( 'NONE', *, *, #26629, .F. ) ;
#27067=VERTEX_POINT ( 'NONE', #22659 ) ;
#27127=DIRECTION ( 'NONE',  ( 0.000000000000000000, 0.000000000000000000, 1.000000000000000000 ) ) ;
#27142=DIRECTION ( 'NONE',  ( 0.000000000000000000, 0.5000000000000004441, -0.8660254037844382635 ) ) ;
#27158=CARTESIAN_POINT ( 'NONE',  ( 1.205771365940050410, 15.58845726811990495, 1.140844902514640588E-16 ) ) ;
#27181=CARTESIAN_POINT ( 'NONE',  ( 0.02815752724870344489, 1.322857909648822439, -13.50000000000000000 ) ) ;
#27312=DIRECTION ( 'NONE',  ( -1.000000000000000000, -0.000000000000000000, -0.000000000000000000 ) ) ;
#27365=DIRECTION ( 'NONE',  ( -1.000000000000000000, -0.000000000000000000, -0.000000000000000000 ) ) ;
#27528=ORIENTED_EDGE ( 'NONE', *, *, #23745, .T. ) ;
#27616=CARTESIAN_POINT ( 'NONE',  ( 0.8377008405913450861, 8.431745484731994367, 12.39578842395470737 ) ) ;
#27660=ORIENTED_EDGE ( 'NONE', *, *, #25737, .F. ) ;
#27707=ORIENTED_EDGE ( 'NONE', *, *, #26715, .T. ) ;
#27721=PRODUCT_DEFINITION ( 'UNKNOWN', '', #25220, #2500 ) ;
#27763=EDGE_CURVE ( 'NONE', #27067, #15570, #5116, .T. ) ;
#27787=DIRECTION ( 'NONE',  ( 1.000000000000000000, 0.000000000000000000, 0.000000000000000000 ) ) ;
#27792=DIRECTION ( 'NONE',  ( 0.000000000000000000, 0.000000000000000000, -1.000000000000000000 ) ) ;
#27798=CARTESIAN_POINT ( 'NONE',  ( 0.1396634953560761672, 2.649662288454536441, 13.50000000000000000 ) ) ;
#27893=ORIENTED_EDGE ( 'NONE', *, *, #15478, .F. ) ;
#27929=AXIS2_PLACEMENT_3D ( 'NONE', #21718, #13893, #24732 ) ;
#27996=VERTEX_POINT ( 'NONE', #676 ) ;
#28026=CARTESIAN_POINT ( 'NONE',  ( 53.89849999999999852, 0.000000000000000000, 0.000000000000000000 ) ) ;
#28042=FACE_OUTER_BOUND ( 'NONE', #25847, .T. ) ;
#28093=DIRECTION ( 'NONE',  ( 0.000000000000000000, 0.000000000000000000, -1.000000000000000000 ) ) ;
#28101=ORIENTED_EDGE ( 'NONE', *, *, #18501, .T. ) ;
#28190=CARTESIAN_POINT ( 'NONE',  ( 10.00000000000000000, 15.58845726811990495, 0.000000000000000000 ) ) ;
#28212=ADVANCED_FACE ( 'NONE', ( #18639 ), #21111, .F. ) ;
#28383=AXIS2_PLACEMENT_3D ( 'NONE', #30718, #6312, #16862 ) ;
#28463=DIRECTION ( 'NONE',  ( 0.000000000000000000, 0.5000000000000007772, -0.8660254037844381525 ) ) ;
#28555=DIRECTION ( 'NONE',  ( 1.000000000000000000, 0.000000000000000000, 0.000000000000000000 ) ) ;
#28566=AXIS2_PLACEMENT_3D ( 'NONE', #26579, #2200, #13073 ) ;
#28588=ORIENTED_EDGE ( 'NONE', *, *, #25046, .F. ) ;
#28704=CARTESIAN_POINT ( 'NONE',  ( 0.1134162231544147831, -2.627030748427853002, 13.50000000000000000 ) ) ;
#28788=EDGE_LOOP ( 'NONE', ( #31629, #9859, #2686 ) ) ;
#28816=ORIENTED_EDGE ( 'NONE', *, *, #18501, .F. ) ;
#28858=ORIENTED_EDGE ( 'NONE', *, *, #23306, .T. ) ;
#28925=DIRECTION ( 'NONE',  ( 0.000000000000000000, 0.000000000000000000, -1.000000000000000000 ) ) ;
#29033=VECTOR ( 'NONE', #27142, 1000.000000000000227 ) ;
#29044=ORIENTED_EDGE ( 'NONE', *, *, #10371, .F. ) ;
#29099=DIRECTION ( 'NONE',  ( 1.000000000000000000, 0.000000000000000000, -0.000000000000000000 ) ) ;
#29141=( GEOMETRIC_REPRESENTATION_CONTEXT ( 3 ) GLOBAL_UNCERTAINTY_ASSIGNED_CONTEXT ( ( #16059 ) ) GLOBAL_UNIT_ASSIGNED_CONTEXT ( ( #29921, #11053, #4990 ) ) REPRESENTATION_CONTEXT ( 'NONE', 'WORKASPACE' ) );
#29153=EDGE_CURVE ( 'NONE', #35009, #10400, #15021, .T. ) ;
#29157=CARTESIAN_POINT ( 'NONE',  ( 0.5328044427895346491, -5.227541351202838804, -13.49999999999999822 ) ) ;
#29250=DIRECTION ( 'NONE',  ( 0.000000000000000000, 0.000000000000000000, 1.000000000000000000 ) ) ;
#29258=CARTESIAN_POINT ( 'NONE',  ( -1.059638217015129409E-14, 11.36060796471277001, -7.322849800245817775 ) ) ;
#29334=CIRCLE ( 'NONE', #10586, 13.50000000000000178 ) ;
#29340=ORIENTED_EDGE ( 'NONE', *, *, #25046, .T. ) ;
#29343=DIRECTION ( 'NONE',  ( -0.7071067811865513475, 8.659560562354884787E-17, -0.7071067811865435759 ) ) ;
#29385=DIRECTION ( 'NONE',  ( 0.000000000000000000, 0.000000000000000000, 1.000000000000000000 ) ) ;
#29484=AXIS2_PLACEMENT_3D ( 'NONE', #2337, #13216, #12514 ) ;
#29492=CARTESIAN_POINT ( 'NONE',  ( 0.5344654698446009711, -9.073918974790316838, -11.28351131189991285 ) ) ;
#29501=CARTESIAN_POINT ( 'NONE',  ( 9.199999999999999289, 13.50000000000000178, 0.000000000000000000 ) ) ;
#29526=AXIS2_PLACEMENT_3D ( 'NONE', #10775, #32119, #26778 ) ;
#29531=DIRECTION ( 'NONE',  ( -1.000000000000000000, -0.000000000000000000, -0.000000000000000000 ) ) ;
#29556=DIRECTION ( 'NONE',  ( -0.000000000000000000, 0.000000000000000000, 1.000000000000000000 ) ) ;
#29596=CARTESIAN_POINT ( 'NONE',  ( 0.000000000000000000, 0.000000000000000000, 0.000000000000000000 ) ) ;
#29761=ORIENTED_EDGE ( 'NONE', *, *, #12173, .T. ) ;
#29767=DIRECTION ( 'NONE',  ( -1.000000000000000000, -0.000000000000000000, -0.000000000000000000 ) ) ;
#29768=FACE_OUTER_BOUND ( 'NONE', #11562, .T. ) ;
#29770=AXIS2_PLACEMENT_3D ( 'NONE', #8564, #3572, #25106 ) ;
#29839=CARTESIAN_POINT ( 'NONE',  ( 1.205771365940050854, -7.794228634059966687, -13.49999999999999822 ) ) ;
#29921=( LENGTH_UNIT ( ) NAMED_UNIT ( * ) SI_UNIT ( .MILLI., .METRE. ) );
#29966=DIRECTION ( 'NONE',  ( -1.000000000000000000, -0.000000000000000000, -0.000000000000000000 ) ) ;
#29985=DIRECTION ( 'NONE',  ( 0.000000000000000000, 0.000000000000000000, -1.000000000000000000 ) ) ;
#30155=ORIENTED_EDGE ( 'NONE', *, *, #16293, .F. ) ;
#30190=AXIS2_PLACEMENT_3D ( 'NONE', #2755, #24635, #18632 ) ;
#30371=EDGE_CURVE ( 'NONE', #23862, #12566, #11703, .T. ) ;
#30651=CARTESIAN_POINT ( 'NONE',  ( 1.205771365940041528, 7.794228634059941818, 13.49999999999999645 ) ) ;
#30670=ORIENTED_EDGE ( 'NONE', *, *, #15478, .T. ) ;
#30674=CARTESIAN_POINT ( 'NONE',  ( 0.000000000000000000, 0.000000000000000000, 8.000000000000000000 ) ) ;
#30688=LINE ( 'NONE', #6461, #17413 ) ;
#30701=FACE_OUTER_BOUND ( 'NONE', #19915, .T. ) ;
#30718=CARTESIAN_POINT ( 'NONE',  ( 10.00000000000000000, -7.794228634059966687, -13.49999999999999822 ) ) ;
#30739=CONICAL_SURFACE ( 'NONE', #7421, 6.898500000000000298, 0.7853981633974428389 ) ;
#30831=VECTOR ( 'NONE', #31813, 1000.000000000000000 ) ;
#30846=ORIENTED_EDGE ( 'NONE', *, *, #17876, .F. ) ;
#30862=CARTESIAN_POINT ( 'NONE',  ( 0.000000000000000000, 11.69134295108991495, 6.750000000000012434 ) ) ;
#30942=DIRECTION ( 'NONE',  ( 1.000000000000000000, 0.000000000000000000, -0.000000000000000000 ) ) ;
#30993=ORIENTED_EDGE ( 'NONE', *, *, #21511, .T. ) ;
#31018=EDGE_CURVE ( 'NONE', #33119, #15570, #202, .T. ) ;
#31125=CARTESIAN_POINT ( 'NONE',  ( 1.205771365940061957, -15.58845726811992449, 7.826847450972439323E-16 ) ) ;
#31253=CARTESIAN_POINT ( 'NONE',  ( 1.205771365940041306, -7.794228634059936489, 13.50000000000000000 ) ) ;
#31337=FACE_OUTER_BOUND ( 'NONE', #7800, .T. ) ;
#31353=VECTOR ( 'NONE', #20244, 1000.000000000000114 ) ;
#31396=DIRECTION ( 'NONE',  ( 0.000000000000000000, 0.000000000000000000, 1.000000000000000000 ) ) ;
#31431=ORIENTED_EDGE ( 'NONE', *, *, #10371, .T. ) ;
#31452=EDGE_CURVE ( 'NONE', #5849, #32902, #4411, .T. ) ;
#31471=EDGE_CURVE ( 'NONE', #19390, #20784, #21148, .T. ) ;
#31522=CARTESIAN_POINT ( 'NONE',  ( 0.8377008405913507483, 14.95094041744785152, -1.104211576045294407 ) ) ;
#31559=CARTESIAN_POINT ( 'NONE',  ( 1.205771365940050410, 15.58845726811990495, 1.140844902514640588E-16 ) ) ;
#31587=ORIENTED_EDGE ( 'NONE', *, *, #14620, .F. ) ;
#31629=ORIENTED_EDGE ( 'NONE', *, *, #5915, .T. ) ;
#31813=DIRECTION ( 'NONE',  ( -1.000000000000000000, -0.000000000000000000, -0.000000000000000000 ) ) ;
#31860=ORIENTED_EDGE ( 'NONE', *, *, #17876, .T. ) ;
#31908=VERTEX_POINT ( 'NONE', #2403 ) ;
#31992=CARTESIAN_POINT ( 'NONE',  ( 0.000000000000000000, 1.653273178848927064E-15, -13.50000000000000178 ) ) ;
#32081=CIRCLE ( 'NONE', #12221, 13.50000000000000178 ) ;
#32091=ADVANCED_FACE ( 'NONE', ( #30701 ), #21798, .T. ) ;
#32114=AXIS2_PLACEMENT_3D ( 'NONE', #10379, #10204, #29250 ) ;
#32115=DIRECTION ( 'NONE',  ( 1.000000000000000000, 0.000000000000000000, 0.000000000000000000 ) ) ;
#32119=DIRECTION ( 'NONE',  ( 0.000000000000000000, 0.8660254037844375974, -0.5000000000000019984 ) ) ;
#32205=EDGE_LOOP ( 'NONE', ( #3337, #11778 ) ) ;
#32217=CARTESIAN_POINT ( 'NONE',  ( 0.02849990174190952102, -12.35429686688394391, -5.601730134768054370 ) ) ;
#32219=FACE_OUTER_BOUND ( 'NONE', #18037, .T. ) ;
#32317=VERTEX_POINT ( 'NONE', #23557 ) ;
#32384=CARTESIAN_POINT ( 'NONE',  ( 0.8386200322165885401, -14.95253250404442902, -1.101454001170013353 ) ) ;
#32436=VECTOR ( 'NONE', #25865, 1000.000000000000000 ) ;
#32498=DIRECTION ( 'NONE',  ( 0.000000000000000000, 0.000000000000000000, -1.000000000000000000 ) ) ;
#32544=DIRECTION ( 'NONE',  ( -0.7071067811865513475, 0.000000000000000000, 0.7071067811865435759 ) ) ;
#32587=VERTEX_POINT ( 'NONE', #936 ) ;
#32652=CARTESIAN_POINT ( 'NONE',  ( 9.199999999999999289, 0.000000000000000000, 0.000000000000000000 ) ) ;
#32700=DIRECTION ( 'NONE',  ( -1.000000000000000000, -0.000000000000000000, -0.000000000000000000 ) ) ;
#32701=VERTEX_POINT ( 'NONE', #18024 ) ;
#32778=PRODUCT ( 'hex structural bolt gradec short_iso_ISO 7412 - M16 x 45 --- 26-WN', 'hex structural bolt gradec short_iso_ISO 7412 - M16 x 45 --- 26-WN', '', ( #7489 ) ) ;
#32827=EDGE_LOOP ( 'NONE', ( #28101, #18872, #19679 ) ) ;
#32898=LINE ( 'NONE', #16200, #12440 ) ;
#32901=AXIS2_PLACEMENT_3D ( 'NONE', #7726, #32115, #28925 ) ;
#32902=VERTEX_POINT ( 'NONE', #14865 ) ;
#32944=CYLINDRICAL_SURFACE ( 'NONE', #29770, 8.000000000000000000 ) ;
#32964=VERTEX_POINT ( 'NONE', #13411 ) ;
#33012=ADVANCED_FACE ( 'NONE', ( #29768 ), #3096, .T. ) ;
#33029=B_SPLINE_CURVE_WITH_KNOTS ( 'NONE', 3,
 ( #29839, #18817, #29492, #8115, #18994, #5439 ),
 .UNSPECIFIED., .F., .F.,
 ( 4, 2, 4 ),
 ( 2.380729204614878139E-07, 0.003943479449179622918, 0.007886720825438783139 ),
 .UNSPECIFIED. ) ;
#33046=EDGE_CURVE ( 'NONE', #20784, #18455, #32081, .T. ) ;
#33075=CIRCLE ( 'NONE', #22854, 13.50000000000000178 ) ;
#33088=DIRECTION ( 'NONE',  ( 0.000000000000000000, 0.000000000000000000, -1.000000000000000000 ) ) ;
#33114=CARTESIAN_POINT ( 'NONE',  ( 9.199999999999999289, -11.69134295108991850, -6.750000000000008882 ) ) ;
#33119=VERTEX_POINT ( 'NONE', #11268 ) ;
#33266=DIRECTION ( 'NONE',  ( -1.000000000000000000, -0.000000000000000000, -0.000000000000000000 ) ) ;
#33322=DIRECTION ( 'NONE',  ( 0.000000000000000000, 0.000000000000000000, 1.000000000000000000 ) ) ;
#33336=ORIENTED_EDGE ( 'NONE', *, *, #8643, .F. ) ;
#33363=CARTESIAN_POINT ( 'NONE',  ( 0.000000000000000000, 0.000000000000000000, 0.000000000000000000 ) ) ;
#33419=ADVANCED_FACE ( 'NONE', ( #34721 ), #10334, .T. ) ;
#33636=ORIENTED_EDGE ( 'NONE', *, *, #480, .F. ) ;
#33641=AXIS2_PLACEMENT_3D ( 'NONE', #20079, #3156, #9394 ) ;
#33646=MANIFOLD_SOLID_BREP ( 'BearingFace', #24161 ) ;
#33685=ADVANCED_FACE ( 'NONE', ( #15084 ), #4368, .F. ) ;
#33701=FACE_BOUND ( 'NONE', #34732, .T. ) ;
#33742=EDGE_CURVE ( 'NONE', #31908, #17794, #9711, .T. ) ;
#33789=EDGE_CURVE ( 'NONE', #18455, #12566, #2891, .T. ) ;
#33840=CARTESIAN_POINT ( 'NONE',  ( 0.1149164202474769469, 10.37169118567825699, 9.035703905990970952 ) ) ;
#33857=CARTESIAN_POINT ( 'NONE',  ( -3.062871137271549632E-15, -12.35529564071043040, 5.600000207755297055 ) ) ;
#33875=CARTESIAN_POINT ( 'NONE',  ( 0.5328044427876279521, -5.227541351193698560, 13.50000000000000178 ) ) ;
#33928=EDGE_CURVE ( 'NONE', #32701, #20439, #19480, .T. ) ;
#33981=B_SPLINE_CURVE_WITH_KNOTS ( 'NONE', 3,
 ( #17146, #755, #3239, #27798, #14114, #3411, #22473, #934 ),
 .UNSPECIFIED., .F., .F.,
 ( 4, 2, 2, 4 ),
 ( 0.02224295563652558400, 0.02421672923683100900, 0.02619050283713643401, 0.03013805003774728056 ),
 .UNSPECIFIED. ) ;
#34044=CARTESIAN_POINT ( 'NONE',  ( 0.000000000000000000, 3.004629197474321612E-15, 13.50000000000000000 ) ) ;
#34103=CARTESIAN_POINT ( 'NONE',  ( 0.000000000000000000, 15.58845726811990673, -2.400813222210650817E-15 ) ) ;
#34106=ORIENTED_EDGE ( 'NONE', *, *, #23745, .F. ) ;
#34133=ORIENTED_EDGE ( 'NONE', *, *, #26715, .F. ) ;
#34233=ORIENTED_EDGE ( 'NONE', *, *, #12842, .F. ) ;
#34320=EDGE_CURVE ( 'NONE', #15570, #17480, #7620, .T. ) ;
#34324=DIRECTION ( 'NONE',  ( 0.000000000000000000, -0.8660254037844382635, -0.5000000000000008882 ) ) ;
#34333=VERTEX_POINT ( 'NONE', #23179 ) ;
#34376=VERTEX_POINT ( 'NONE', #4985 ) ;
#34405=DIRECTION ( 'NONE',  ( -0.000000000000000000, 0.000000000000000000, -1.000000000000000000 ) ) ;
#34460=DIRECTION ( 'NONE',  ( 0.000000000000000000, 0.000000000000000000, -1.000000000000000000 ) ) ;
#34501=CARTESIAN_POINT ( 'NONE',  ( 10.00000000000000000, 15.58845726811990495, 0.000000000000000000 ) ) ;
#34599=CARTESIAN_POINT ( 'NONE',  ( 0.000000000000000000, 11.69134295108991140, -6.750000000000015987 ) ) ;
#34621=FACE_OUTER_BOUND ( 'NONE', #12984, .T. ) ;
#34685=CARTESIAN_POINT ( 'NONE',  ( 9.199999999999999289, 7.794228634059932048, -13.49999999999999822 ) ) ;
#34717=EDGE_CURVE ( 'NONE', #14536, #19390, #33075, .T. ) ;
#34721=FACE_OUTER_BOUND ( 'NONE', #28788, .T. ) ;
#34732=EDGE_LOOP ( 'NONE', ( #19751, #26671 ) ) ;
#34739=AXIS2_PLACEMENT_3D ( 'NONE', #34103, #15259, #9721 ) ;
#34759=EDGE_CURVE ( 'NONE', #11327, #20784, #26494, .T. ) ;
#34798=AXIS2_PLACEMENT_3D ( 'NONE', #34501, #34324, #28463 ) ;
#34897=DIRECTION ( 'NONE',  ( 0.000000000000000000, -0.5000000000000012212, -0.8660254037844380415 ) ) ;
#34968=VECTOR ( 'NONE', #32544, 1000.000000000000114 ) ;
#35009=VERTEX_POINT ( 'NONE', #3336 ) ;
#35047=DIRECTION ( 'NONE',  ( 0.000000000000000000, 0.000000000000000000, -1.000000000000000000 ) ) ;
#35063=CARTESIAN_POINT ( 'NONE',  ( 10.00000000000000000, 0.000000000000000000, 0.000000000000000000 ) ) ;
#35276=COLOUR_RGB('Black',0.12,0.14,0.17);
#35277=FILL_AREA_STYLE_COLOUR('',#35276);
#35278=FILL_AREA_STYLE('',(#35277));
#35279=SURFACE_STYLE_FILL_AREA(#35278);
#35280=SURFACE_SIDE_STYLE('',(#35279));
#35281=SURFACE_STYLE_USAGE(.BOTH.,#35280);
#35282=PRESENTATION_STYLE_ASSIGNMENT((#35281));
ENDSEC;
END-ISO-10303-21;
